ISO-10303-21;
HEADER;
/* Generated by software containing ST-Developer
 * from STEP Tools, Inc. (www.steptools.com) 
 */

FILE_DESCRIPTION(
/* description */ (''),
/* implementation_level */ '2;1');

FILE_NAME(
/* name */ 'Crank_01.step',
/* time_stamp */ '2026-09-20T21:58:27+06:00',
/* author */ (''),
/* organization */ (''),
/* preprocessor_version */ 'ST-DEVELOPER v20.2',
/* originating_system */ 'Autodesk Translation Framework v15.15.0.0',
/* authorisation */ '');

FILE_SCHEMA (('AUTOMOTIVE_DESIGN { 1 0 10303 214 3 1 1 }'));
ENDSEC;

DATA;
#10=MECHANICAL_DESIGN_GEOMETRIC_PRESENTATION_REPRESENTATION('',(#62),#2238);
#46=SHAPE_REPRESENTATION_RELATIONSHIP('SRR','None',#2273,#54);
#54=ADVANCED_BREP_SHAPE_REPRESENTATION('',(#70),#2233);
#62=STYLED_ITEM('',(#2320),#70);
#70=MANIFOLD_SOLID_BREP('Crank_01',#1209);
#77=FACE_BOUND('',#239,.T.);
#78=FACE_BOUND('',#242,.T.);
#107=PLANE('',#1410);
#108=PLANE('',#1414);
#166=FACE_OUTER_BOUND('',#237,.T.);
#167=FACE_OUTER_BOUND('',#238,.T.);
#168=FACE_OUTER_BOUND('',#240,.T.);
#169=FACE_OUTER_BOUND('',#241,.T.);
#237=EDGE_LOOP('',(#1016,#1017,#1018,#1019));
#238=EDGE_LOOP('',(#1020));
#239=EDGE_LOOP('',(#1021));
#240=EDGE_LOOP('',(#1022,#1023,#1024,#1025));
#241=EDGE_LOOP('',(#1026));
#242=EDGE_LOOP('',(#1027));
#336=LINE('',#2117,#421);
#337=LINE('',#2124,#422);
#421=VECTOR('',#1738,2.5);
#422=VECTOR('',#1747,13.);
#497=CIRCLE('',#1408,2.5);
#498=CIRCLE('',#1409,2.5);
#499=CIRCLE('',#1411,13.);
#500=CIRCLE('',#1413,13.);
#595=VERTEX_POINT('',#2114);
#596=VERTEX_POINT('',#2116);
#597=VERTEX_POINT('',#2120);
#598=VERTEX_POINT('',#2123);
#740=EDGE_CURVE('',#595,#595,#497,.T.);
#741=EDGE_CURVE('',#595,#596,#336,.T.);
#742=EDGE_CURVE('',#596,#596,#498,.T.);
#743=EDGE_CURVE('',#597,#597,#499,.T.);
#744=EDGE_CURVE('',#597,#598,#337,.T.);
#745=EDGE_CURVE('',#598,#598,#500,.T.);
#1016=ORIENTED_EDGE('',*,*,#740,.F.);
#1017=ORIENTED_EDGE('',*,*,#741,.T.);
#1018=ORIENTED_EDGE('',*,*,#742,.F.);
#1019=ORIENTED_EDGE('',*,*,#741,.F.);
#1020=ORIENTED_EDGE('',*,*,#743,.T.);
#1021=ORIENTED_EDGE('',*,*,#742,.T.);
#1022=ORIENTED_EDGE('',*,*,#743,.F.);
#1023=ORIENTED_EDGE('',*,*,#744,.T.);
#1024=ORIENTED_EDGE('',*,*,#745,.T.);
#1025=ORIENTED_EDGE('',*,*,#744,.F.);
#1026=ORIENTED_EDGE('',*,*,#745,.F.);
#1027=ORIENTED_EDGE('',*,*,#740,.T.);
#1127=CYLINDRICAL_SURFACE('',#1407,2.5);
#1128=CYLINDRICAL_SURFACE('',#1412,13.);
#1182=ADVANCED_FACE('',(#166),#1127,.F.);
#1183=ADVANCED_FACE('',(#167,#77),#107,.F.);
#1184=ADVANCED_FACE('',(#168),#1128,.T.);
#1185=ADVANCED_FACE('',(#169,#78),#108,.T.);
#1209=CLOSED_SHELL('',(#1182,#1183,#1184,#1185));
#1406=AXIS2_PLACEMENT_3D('',#2112,#1732,#1733);
#1407=AXIS2_PLACEMENT_3D('',#2113,#1734,#1735);
#1408=AXIS2_PLACEMENT_3D('',#2115,#1736,#1737);
#1409=AXIS2_PLACEMENT_3D('',#2118,#1739,#1740);
#1410=AXIS2_PLACEMENT_3D('',#2119,#1741,#1742);
#1411=AXIS2_PLACEMENT_3D('',#2121,#1743,#1744);
#1412=AXIS2_PLACEMENT_3D('',#2122,#1745,#1746);
#1413=AXIS2_PLACEMENT_3D('',#2125,#1748,#1749);
#1414=AXIS2_PLACEMENT_3D('',#2126,#1750,#1751);
#1732=DIRECTION('axis',(0.,0.,1.));
#1733=DIRECTION('refdir',(1.,0.,0.));
#1734=DIRECTION('center_axis',(0.,1.,0.));
#1735=DIRECTION('ref_axis',(1.,0.,0.));
#1736=DIRECTION('center_axis',(0.,-1.,0.));
#1737=DIRECTION('ref_axis',(1.,0.,0.));
#1738=DIRECTION('',(0.,-1.,0.));
#1739=DIRECTION('center_axis',(0.,1.,0.));
#1740=DIRECTION('ref_axis',(1.,0.,0.));
#1741=DIRECTION('center_axis',(0.,1.,0.));
#1742=DIRECTION('ref_axis',(1.,0.,0.));
#1743=DIRECTION('center_axis',(0.,-1.,0.));
#1744=DIRECTION('ref_axis',(1.,0.,0.));
#1745=DIRECTION('center_axis',(0.,-1.,0.));
#1746=DIRECTION('ref_axis',(1.,0.,0.));
#1747=DIRECTION('',(0.,1.,0.));
#1748=DIRECTION('center_axis',(0.,-1.,0.));
#1749=DIRECTION('ref_axis',(1.,0.,0.));
#1750=DIRECTION('center_axis',(0.,1.,0.));
#1751=DIRECTION('ref_axis',(1.,0.,0.));
#2112=CARTESIAN_POINT('',(0.,0.,0.));
#2113=CARTESIAN_POINT('Origin',(0.,0.,24.1717785126239));
#2114=CARTESIAN_POINT('',(-2.5,3.,24.1717785126239));
#2115=CARTESIAN_POINT('Origin',(0.,3.,24.1717785126239));
#2116=CARTESIAN_POINT('',(-2.5,-5.,24.1717785126239));
#2117=CARTESIAN_POINT('',(-2.5,0.,24.1717785126239));
#2118=CARTESIAN_POINT('Origin',(0.,-5.,24.1717785126239));
#2119=CARTESIAN_POINT('Origin',(0.,-5.,24.1717785126239));
#2120=CARTESIAN_POINT('',(-13.,-5.,24.1717785126239));
#2121=CARTESIAN_POINT('Origin',(0.,-5.,24.1717785126239));
#2122=CARTESIAN_POINT('Origin',(0.,0.,24.1717785126239));
#2123=CARTESIAN_POINT('',(-13.,3.,24.1717785126239));
#2124=CARTESIAN_POINT('',(-13.,0.,24.1717785126239));
#2125=CARTESIAN_POINT('Origin',(0.,3.,24.1717785126239));
#2126=CARTESIAN_POINT('Origin',(0.,3.,24.1717785126239));
#2223=UNCERTAINTY_MEASURE_WITH_UNIT(LENGTH_MEASURE(0.01),#2239,
'DISTANCE_ACCURACY_VALUE',
'Maximum model space distance between geometric entities at asserted c
onnectivities');
#2228=UNCERTAINTY_MEASURE_WITH_UNIT(LENGTH_MEASURE(0.01),#2239,
'DISTANCE_ACCURACY_VALUE',
'Maximum model space distance between geometric entities at asserted c
onnectivities');
#2233=(
GEOMETRIC_REPRESENTATION_CONTEXT(3)
GLOBAL_UNCERTAINTY_ASSIGNED_CONTEXT((#2223))
GLOBAL_UNIT_ASSIGNED_CONTEXT((#2239,#2241,#2242))
REPRESENTATION_CONTEXT('','3D')
);
#2238=(
GEOMETRIC_REPRESENTATION_CONTEXT(3)
GLOBAL_UNCERTAINTY_ASSIGNED_CONTEXT((#2228))
GLOBAL_UNIT_ASSIGNED_CONTEXT((#2239,#2241,#2242))
REPRESENTATION_CONTEXT('','3D')
);
#2239=(
LENGTH_UNIT()
NAMED_UNIT(*)
SI_UNIT(.MILLI.,.METRE.)
);
#2241=(
NAMED_UNIT(*)
PLANE_ANGLE_UNIT()
SI_UNIT($,.RADIAN.)
);
#2242=(
NAMED_UNIT(*)
SI_UNIT($,.STERADIAN.)
SOLID_ANGLE_UNIT()
);
#2247=SHAPE_DEFINITION_REPRESENTATION(#2256,#2273);
#2256=PRODUCT_DEFINITION_SHAPE('',$,#2283);
#2273=SHAPE_REPRESENTATION('',(#1406),#2233);
#2278=PRODUCT_DEFINITION_CONTEXT('part definition',#2307,'design');
#2283=PRODUCT_DEFINITION('Crank_01','Crank_01',#2292,#2278);
#2292=PRODUCT_DEFINITION_FORMATION('',$,#2313);
#2307=APPLICATION_CONTEXT(
'Core Data for Automotive Mechanical Design Process');
#2308=PRODUCT_CONTEXT('part definition',#2307,'mechanical');
#2313=PRODUCT('Crank_01','Crank_01',$,(#2308));
#2320=PRESENTATION_STYLE_ASSIGNMENT((#2324));
#2324=SURFACE_STYLE_USAGE(.BOTH.,#2328);
#2328=SURFACE_SIDE_STYLE('',(#2332));
#2332=SURFACE_STYLE_FILL_AREA(#2336);
#2336=FILL_AREA_STYLE('Surface - Matte',(#2340));
#2340=FILL_AREA_STYLE_COLOUR('Surface - Matte',#2344);
#2344=COLOUR_RGB('Surface - Matte', 0.66274510, 0.83137255, 0.94901961);
ENDSEC;
END-ISO-10303-21;
